ISO-10303-21;
HEADER;
/* Generated by software containing ST-Developer
 * from STEP Tools, Inc. (www.steptools.com) 
 */

FILE_DESCRIPTION(
/* description */ ('PAT-091'),
/* implementation_level */ '2;1');

FILE_NAME(
/* name */ 'Cap Screw - M4x16.step',
/* time_stamp */ '2026-10-27T15:34:44-07:00',
/* author */ (''),
/* organization */ (''),
/* preprocessor_version */ 'ST-DEVELOPER v20.2',
/* originating_system */ 'Autodesk Translation Framework v15.17.0.0',
/* authorisation */ '');

FILE_SCHEMA (('AUTOMOTIVE_DESIGN { 1 0 10303 214 3 1 1 }'));
ENDSEC;

DATA;
#10=MECHANICAL_DESIGN_GEOMETRIC_PRESENTATION_REPRESENTATION('',(#1043),#25100);
#737=CONICAL_SURFACE('',#15676,0.325,0.785398163397448);
#738=CONICAL_SURFACE('',#15680,0.335,0.785398163397448);
#739=CONICAL_SURFACE('',#15684,0.21,0.463647609000806);
#740=CONICAL_SURFACE('',#15688,0.18,0.785398163397448);
#747=ORIENTED_CLOSED_SHELL('',*,#13323,.F.);
#750=BREP_WITH_VOIDS('Body1',#13322,(#747));
#823=SHAPE_REPRESENTATION_RELATIONSHIP('SRR','None',#25589,#933);
#933=ADVANCED_BREP_SHAPE_REPRESENTATION('',(#750),#25059);
#1043=STYLED_ITEM('',(#26198),#750);
#1524=FACE_BOUND('',#3728,.T.);
#1937=PLANE('',#15674);
#1938=PLANE('',#15682);
#1939=PLANE('',#15690);
#1940=PLANE('',#15691);
#1941=PLANE('',#15692);
#1942=PLANE('',#15693);
#1943=PLANE('',#15694);
#1944=PLANE('',#15695);
#1945=PLANE('',#15696);
#1946=PLANE('',#15697);
#1947=PLANE('',#15698);
#2596=FACE_OUTER_BOUND('',#3723,.T.);
#2597=FACE_OUTER_BOUND('',#3724,.T.);
#2598=FACE_OUTER_BOUND('',#3725,.T.);
#2599=FACE_OUTER_BOUND('',#3726,.T.);
#2600=FACE_OUTER_BOUND('',#3727,.T.);
#2601=FACE_OUTER_BOUND('',#3729,.T.);
#2602=FACE_OUTER_BOUND('',#3730,.T.);
#2603=FACE_OUTER_BOUND('',#3731,.T.);
#2604=FACE_OUTER_BOUND('',#3732,.T.);
#2605=FACE_OUTER_BOUND('',#3733,.T.);
#2606=FACE_OUTER_BOUND('',#3734,.T.);
#2607=FACE_OUTER_BOUND('',#3735,.T.);
#2608=FACE_OUTER_BOUND('',#3736,.T.);
#2609=FACE_OUTER_BOUND('',#3737,.T.);
#2610=FACE_OUTER_BOUND('',#3738,.T.);
#2611=FACE_OUTER_BOUND('',#3739,.T.);
#2612=FACE_OUTER_BOUND('',#3740,.T.);
#3723=EDGE_LOOP('',(#11080));
#3724=EDGE_LOOP('',(#11081,#11082,#11083,#11084));
#3725=EDGE_LOOP('',(#11085,#11086,#11087,#11088));
#3726=EDGE_LOOP('',(#11089,#11090,#11091,#11092));
#3727=EDGE_LOOP('',(#11093));
#3728=EDGE_LOOP('',(#11094));
#3729=EDGE_LOOP('',(#11095,#11096,#11097,#11098));
#3730=EDGE_LOOP('',(#11099,#11100,#11101,#11102));
#3731=EDGE_LOOP('',(#11103,#11104,#11105,#11106));
#3732=EDGE_LOOP('',(#11107));
#3733=EDGE_LOOP('',(#11108,#11109,#11110,#11111));
#3734=EDGE_LOOP('',(#11112,#11113,#11114,#11115));
#3735=EDGE_LOOP('',(#11116,#11117,#11118,#11119));
#3736=EDGE_LOOP('',(#11120,#11121,#11122,#11123));
#3737=EDGE_LOOP('',(#11124,#11125,#11126,#11127));
#3738=EDGE_LOOP('',(#11128,#11129,#11130,#11131));
#3739=EDGE_LOOP('',(#11132,#11133,#11134,#11135,#11136,#11137));
#3740=EDGE_LOOP('',(#11138,#11139,#11140,#11141,#11142,#11143));
#4700=LINE('',#23401,#5440);
#4701=LINE('',#23405,#5441);
#4702=LINE('',#23409,#5442);
#4703=LINE('',#23416,#5443);
#4704=LINE('',#23420,#5444);
#4705=LINE('',#23424,#5445);
#4706=LINE('',#23429,#5446);
#4707=LINE('',#23431,#5447);
#4708=LINE('',#23433,#5448);
#4709=LINE('',#23434,#5449);
#4710=LINE('',#23437,#5450);
#4711=LINE('',#23439,#5451);
#4712=LINE('',#23440,#5452);
#4713=LINE('',#23443,#5453);
#4714=LINE('',#23445,#5454);
#4715=LINE('',#23446,#5455);
#4716=LINE('',#23449,#5456);
#4717=LINE('',#23451,#5457);
#4718=LINE('',#23452,#5458);
#4719=LINE('',#23455,#5459);
#4720=LINE('',#23457,#5460);
#4721=LINE('',#23458,#5461);
#4722=LINE('',#23460,#5462);
#4723=LINE('',#23461,#5463);
#5440=VECTOR('',#19230,0.325);
#5441=VECTOR('',#19235,0.35);
#5442=VECTOR('',#19240,0.335);
#5443=VECTOR('',#19249,0.21);
#5444=VECTOR('',#19254,0.2);
#5445=VECTOR('',#19259,0.18);
#5446=VECTOR('',#19264,1.);
#5447=VECTOR('',#19265,1.);
#5448=VECTOR('',#19266,1.);
#5449=VECTOR('',#19267,1.);
#5450=VECTOR('',#19270,1.);
#5451=VECTOR('',#19271,1.);
#5452=VECTOR('',#19272,1.);
#5453=VECTOR('',#19275,1.);
#5454=VECTOR('',#19276,1.);
#5455=VECTOR('',#19277,1.);
#5456=VECTOR('',#19280,1.);
#5457=VECTOR('',#19281,1.);
#5458=VECTOR('',#19282,1.);
#5459=VECTOR('',#19285,1.);
#5460=VECTOR('',#19286,1.);
#5461=VECTOR('',#19287,1.);
#5462=VECTOR('',#19290,1.);
#5463=VECTOR('',#19291,1.);
#6078=CIRCLE('',#15675,0.3);
#6079=CIRCLE('',#15677,0.35);
#6080=CIRCLE('',#15679,0.35);
#6081=CIRCLE('',#15681,0.32);
#6082=CIRCLE('',#15683,0.22);
#6083=CIRCLE('',#15685,0.1954);
#6084=CIRCLE('',#15687,0.1954);
#6085=CIRCLE('',#15689,0.16);
#7083=VERTEX_POINT('',#23396);
#7084=VERTEX_POINT('',#23399);
#7085=VERTEX_POINT('',#23403);
#7086=VERTEX_POINT('',#23407);
#7087=VERTEX_POINT('',#23411);
#7088=VERTEX_POINT('',#23414);
#7089=VERTEX_POINT('',#23418);
#7090=VERTEX_POINT('',#23422);
#7091=VERTEX_POINT('',#23427);
#7092=VERTEX_POINT('',#23428);
#7093=VERTEX_POINT('',#23430);
#7094=VERTEX_POINT('',#23432);
#7095=VERTEX_POINT('',#23436);
#7096=VERTEX_POINT('',#23438);
#7097=VERTEX_POINT('',#23442);
#7098=VERTEX_POINT('',#23444);
#7099=VERTEX_POINT('',#23448);
#7100=VERTEX_POINT('',#23450);
#7101=VERTEX_POINT('',#23454);
#7102=VERTEX_POINT('',#23456);
#8475=EDGE_CURVE('',#7083,#7083,#6078,.T.);
#8476=EDGE_CURVE('',#7084,#7084,#6079,.T.);
#8477=EDGE_CURVE('',#7084,#7083,#4700,.T.);
#8478=EDGE_CURVE('',#7085,#7085,#6080,.T.);
#8479=EDGE_CURVE('',#7085,#7084,#4701,.T.);
#8480=EDGE_CURVE('',#7086,#7086,#6081,.T.);
#8481=EDGE_CURVE('',#7086,#7085,#4702,.T.);
#8482=EDGE_CURVE('',#7087,#7087,#6082,.T.);
#8483=EDGE_CURVE('',#7088,#7088,#6083,.F.);
#8484=EDGE_CURVE('',#7088,#7087,#4703,.T.);
#8485=EDGE_CURVE('',#7089,#7089,#6084,.F.);
#8486=EDGE_CURVE('',#7089,#7088,#4704,.T.);
#8487=EDGE_CURVE('',#7090,#7090,#6085,.T.);
#8488=EDGE_CURVE('',#7090,#7089,#4705,.T.);
#8489=EDGE_CURVE('',#7091,#7092,#4706,.T.);
#8490=EDGE_CURVE('',#7092,#7093,#4707,.T.);
#8491=EDGE_CURVE('',#7093,#7094,#4708,.T.);
#8492=EDGE_CURVE('',#7091,#7094,#4709,.T.);
#8493=EDGE_CURVE('',#7092,#7095,#4710,.T.);
#8494=EDGE_CURVE('',#7095,#7096,#4711,.T.);
#8495=EDGE_CURVE('',#7096,#7093,#4712,.T.);
#8496=EDGE_CURVE('',#7095,#7097,#4713,.T.);
#8497=EDGE_CURVE('',#7097,#7098,#4714,.T.);
#8498=EDGE_CURVE('',#7098,#7096,#4715,.T.);
#8499=EDGE_CURVE('',#7097,#7099,#4716,.T.);
#8500=EDGE_CURVE('',#7099,#7100,#4717,.T.);
#8501=EDGE_CURVE('',#7100,#7098,#4718,.T.);
#8502=EDGE_CURVE('',#7099,#7101,#4719,.T.);
#8503=EDGE_CURVE('',#7101,#7102,#4720,.T.);
#8504=EDGE_CURVE('',#7102,#7100,#4721,.T.);
#8505=EDGE_CURVE('',#7101,#7091,#4722,.T.);
#8506=EDGE_CURVE('',#7094,#7102,#4723,.T.);
#11080=ORIENTED_EDGE('',*,*,#8475,.F.);
#11081=ORIENTED_EDGE('',*,*,#8476,.F.);
#11082=ORIENTED_EDGE('',*,*,#8477,.T.);
#11083=ORIENTED_EDGE('',*,*,#8475,.T.);
#11084=ORIENTED_EDGE('',*,*,#8477,.F.);
#11085=ORIENTED_EDGE('',*,*,#8478,.F.);
#11086=ORIENTED_EDGE('',*,*,#8479,.T.);
#11087=ORIENTED_EDGE('',*,*,#8476,.T.);
#11088=ORIENTED_EDGE('',*,*,#8479,.F.);
#11089=ORIENTED_EDGE('',*,*,#8480,.F.);
#11090=ORIENTED_EDGE('',*,*,#8481,.T.);
#11091=ORIENTED_EDGE('',*,*,#8478,.T.);
#11092=ORIENTED_EDGE('',*,*,#8481,.F.);
#11093=ORIENTED_EDGE('',*,*,#8480,.T.);
#11094=ORIENTED_EDGE('',*,*,#8482,.F.);
#11095=ORIENTED_EDGE('',*,*,#8483,.F.);
#11096=ORIENTED_EDGE('',*,*,#8484,.T.);
#11097=ORIENTED_EDGE('',*,*,#8482,.T.);
#11098=ORIENTED_EDGE('',*,*,#8484,.F.);
#11099=ORIENTED_EDGE('',*,*,#8485,.F.);
#11100=ORIENTED_EDGE('',*,*,#8486,.T.);
#11101=ORIENTED_EDGE('',*,*,#8483,.T.);
#11102=ORIENTED_EDGE('',*,*,#8486,.F.);
#11103=ORIENTED_EDGE('',*,*,#8487,.F.);
#11104=ORIENTED_EDGE('',*,*,#8488,.T.);
#11105=ORIENTED_EDGE('',*,*,#8485,.T.);
#11106=ORIENTED_EDGE('',*,*,#8488,.F.);
#11107=ORIENTED_EDGE('',*,*,#8487,.T.);
#11108=ORIENTED_EDGE('',*,*,#8489,.T.);
#11109=ORIENTED_EDGE('',*,*,#8490,.T.);
#11110=ORIENTED_EDGE('',*,*,#8491,.T.);
#11111=ORIENTED_EDGE('',*,*,#8492,.F.);
#11112=ORIENTED_EDGE('',*,*,#8493,.T.);
#11113=ORIENTED_EDGE('',*,*,#8494,.T.);
#11114=ORIENTED_EDGE('',*,*,#8495,.T.);
#11115=ORIENTED_EDGE('',*,*,#8490,.F.);
#11116=ORIENTED_EDGE('',*,*,#8496,.T.);
#11117=ORIENTED_EDGE('',*,*,#8497,.T.);
#11118=ORIENTED_EDGE('',*,*,#8498,.T.);
#11119=ORIENTED_EDGE('',*,*,#8494,.F.);
#11120=ORIENTED_EDGE('',*,*,#8499,.T.);
#11121=ORIENTED_EDGE('',*,*,#8500,.T.);
#11122=ORIENTED_EDGE('',*,*,#8501,.T.);
#11123=ORIENTED_EDGE('',*,*,#8497,.F.);
#11124=ORIENTED_EDGE('',*,*,#8502,.T.);
#11125=ORIENTED_EDGE('',*,*,#8503,.T.);
#11126=ORIENTED_EDGE('',*,*,#8504,.T.);
#11127=ORIENTED_EDGE('',*,*,#8500,.F.);
#11128=ORIENTED_EDGE('',*,*,#8505,.T.);
#11129=ORIENTED_EDGE('',*,*,#8492,.T.);
#11130=ORIENTED_EDGE('',*,*,#8506,.T.);
#11131=ORIENTED_EDGE('',*,*,#8503,.F.);
#11132=ORIENTED_EDGE('',*,*,#8505,.F.);
#11133=ORIENTED_EDGE('',*,*,#8502,.F.);
#11134=ORIENTED_EDGE('',*,*,#8499,.F.);
#11135=ORIENTED_EDGE('',*,*,#8496,.F.);
#11136=ORIENTED_EDGE('',*,*,#8493,.F.);
#11137=ORIENTED_EDGE('',*,*,#8489,.F.);
#11138=ORIENTED_EDGE('',*,*,#8506,.F.);
#11139=ORIENTED_EDGE('',*,*,#8491,.F.);
#11140=ORIENTED_EDGE('',*,*,#8495,.F.);
#11141=ORIENTED_EDGE('',*,*,#8498,.F.);
#11142=ORIENTED_EDGE('',*,*,#8501,.F.);
#11143=ORIENTED_EDGE('',*,*,#8504,.F.);
#12302=CYLINDRICAL_SURFACE('',#15678,0.35);
#12303=CYLINDRICAL_SURFACE('',#15686,0.1954);
#12963=ADVANCED_FACE('',(#2596),#1937,.T.);
#12964=ADVANCED_FACE('',(#2597),#737,.T.);
#12965=ADVANCED_FACE('',(#2598),#12302,.T.);
#12966=ADVANCED_FACE('',(#2599),#738,.T.);
#12967=ADVANCED_FACE('',(#2600,#1524),#1938,.T.);
#12968=ADVANCED_FACE('',(#2601),#739,.T.);
#12969=ADVANCED_FACE('',(#2602),#12303,.T.);
#12970=ADVANCED_FACE('',(#2603),#740,.T.);
#12971=ADVANCED_FACE('',(#2604),#1939,.T.);
#12972=ADVANCED_FACE('',(#2605),#1940,.F.);
#12973=ADVANCED_FACE('',(#2606),#1941,.F.);
#12974=ADVANCED_FACE('',(#2607),#1942,.F.);
#12975=ADVANCED_FACE('',(#2608),#1943,.F.);
#12976=ADVANCED_FACE('',(#2609),#1944,.F.);
#12977=ADVANCED_FACE('',(#2610),#1945,.F.);
#12978=ADVANCED_FACE('',(#2611),#1946,.F.);
#12979=ADVANCED_FACE('',(#2612),#1947,.F.);
#13322=CLOSED_SHELL('',(#12963,#12964,#12965,#12966,#12967,#12968,#12969,
#12970,#12971));
#13323=CLOSED_SHELL('',(#12972,#12973,#12974,#12975,#12976,#12977,#12978,
#12979));
#15673=AXIS2_PLACEMENT_3D('',#23394,#19220,#19221);
#15674=AXIS2_PLACEMENT_3D('',#23395,#19222,#19223);
#15675=AXIS2_PLACEMENT_3D('',#23397,#19224,#19225);
#15676=AXIS2_PLACEMENT_3D('',#23398,#19226,#19227);
#15677=AXIS2_PLACEMENT_3D('',#23400,#19228,#19229);
#15678=AXIS2_PLACEMENT_3D('',#23402,#19231,#19232);
#15679=AXIS2_PLACEMENT_3D('',#23404,#19233,#19234);
#15680=AXIS2_PLACEMENT_3D('',#23406,#19236,#19237);
#15681=AXIS2_PLACEMENT_3D('',#23408,#19238,#19239);
#15682=AXIS2_PLACEMENT_3D('',#23410,#19241,#19242);
#15683=AXIS2_PLACEMENT_3D('',#23412,#19243,#19244);
#15684=AXIS2_PLACEMENT_3D('',#23413,#19245,#19246);
#15685=AXIS2_PLACEMENT_3D('',#23415,#19247,#19248);
#15686=AXIS2_PLACEMENT_3D('',#23417,#19250,#19251);
#15687=AXIS2_PLACEMENT_3D('',#23419,#19252,#19253);
#15688=AXIS2_PLACEMENT_3D('',#23421,#19255,#19256);
#15689=AXIS2_PLACEMENT_3D('',#23423,#19257,#19258);
#15690=AXIS2_PLACEMENT_3D('',#23425,#19260,#19261);
#15691=AXIS2_PLACEMENT_3D('',#23426,#19262,#19263);
#15692=AXIS2_PLACEMENT_3D('',#23435,#19268,#19269);
#15693=AXIS2_PLACEMENT_3D('',#23441,#19273,#19274);
#15694=AXIS2_PLACEMENT_3D('',#23447,#19278,#19279);
#15695=AXIS2_PLACEMENT_3D('',#23453,#19283,#19284);
#15696=AXIS2_PLACEMENT_3D('',#23459,#19288,#19289);
#15697=AXIS2_PLACEMENT_3D('',#23462,#19292,#19293);
#15698=AXIS2_PLACEMENT_3D('',#23463,#19294,#19295);
#19220=DIRECTION('axis',(0.,0.,1.));
#19221=DIRECTION('refdir',(1.,0.,0.));
#19222=DIRECTION('center_axis',(0.,1.,0.));
#19223=DIRECTION('ref_axis',(0.,0.,1.));
#19224=DIRECTION('center_axis',(0.,-1.,0.));
#19225=DIRECTION('ref_axis',(1.,0.,0.));
#19226=DIRECTION('center_axis',(0.,-1.,0.));
#19227=DIRECTION('ref_axis',(1.,0.,0.));
#19228=DIRECTION('center_axis',(0.,-1.,0.));
#19229=DIRECTION('ref_axis',(1.,0.,0.));
#19230=DIRECTION('',(0.707106781186547,0.707106781186548,8.65956056235493E-17));
#19231=DIRECTION('center_axis',(0.,-1.,0.));
#19232=DIRECTION('ref_axis',(1.,0.,0.));
#19233=DIRECTION('center_axis',(0.,-1.,0.));
#19234=DIRECTION('ref_axis',(1.,0.,0.));
#19235=DIRECTION('',(0.,1.,0.));
#19236=DIRECTION('center_axis',(0.,1.,0.));
#19237=DIRECTION('ref_axis',(1.,0.,0.));
#19238=DIRECTION('center_axis',(0.,-1.,0.));
#19239=DIRECTION('ref_axis',(1.,0.,0.));
#19240=DIRECTION('',(-0.707106781186547,0.707106781186548,-8.65956056235493E-17));
#19241=DIRECTION('center_axis',(0.,-1.,0.));
#19242=DIRECTION('ref_axis',(0.,0.,-1.));
#19243=DIRECTION('center_axis',(0.,-1.,0.));
#19244=DIRECTION('ref_axis',(1.,0.,0.));
#19245=DIRECTION('center_axis',(0.,1.,0.));
#19246=DIRECTION('ref_axis',(1.,0.,0.));
#19247=DIRECTION('center_axis',(0.,1.,0.));
#19248=DIRECTION('ref_axis',(1.,0.,0.));
#19249=DIRECTION('',(-0.447213595499958,0.894427190999916,-5.47678698264203E-17));
#19250=DIRECTION('center_axis',(0.,-1.,0.));
#19251=DIRECTION('ref_axis',(1.,0.,0.));
#19252=DIRECTION('center_axis',(0.,1.,0.));
#19253=DIRECTION('ref_axis',(1.,0.,0.));
#19254=DIRECTION('',(0.,1.,0.));
#19255=DIRECTION('center_axis',(0.,1.,0.));
#19256=DIRECTION('ref_axis',(1.,0.,0.));
#19257=DIRECTION('center_axis',(0.,-1.,0.));
#19258=DIRECTION('ref_axis',(1.,0.,0.));
#19259=DIRECTION('',(-0.707106781186547,0.707106781186548,-8.65956056235493E-17));
#19260=DIRECTION('center_axis',(0.,-1.,0.));
#19261=DIRECTION('ref_axis',(0.,0.,-1.));
#19262=DIRECTION('center_axis',(0.866025403784439,0.,-0.5));
#19263=DIRECTION('ref_axis',(0.5,0.,0.866025403784439));
#19264=DIRECTION('',(-0.5,0.,-0.866025403784439));
#19265=DIRECTION('',(0.,-1.,0.));
#19266=DIRECTION('',(0.5,0.,0.866025403784439));
#19267=DIRECTION('',(0.,-1.,0.));
#19268=DIRECTION('center_axis',(1.60246890531964E-16,0.,-1.));
#19269=DIRECTION('ref_axis',(1.,0.,1.60246890531964E-16));
#19270=DIRECTION('',(-1.,0.,-1.60246890531964E-16));
#19271=DIRECTION('',(0.,-1.,0.));
#19272=DIRECTION('',(1.,0.,1.60246890531964E-16));
#19273=DIRECTION('center_axis',(-0.866025403784439,0.,-0.5));
#19274=DIRECTION('ref_axis',(0.5,0.,-0.866025403784439));
#19275=DIRECTION('',(-0.5,0.,0.866025403784439));
#19276=DIRECTION('',(0.,-1.,0.));
#19277=DIRECTION('',(0.5,0.,-0.866025403784439));
#19278=DIRECTION('center_axis',(-0.866025403784439,0.,0.5));
#19279=DIRECTION('ref_axis',(-0.5,0.,-0.866025403784439));
#19280=DIRECTION('',(0.5,0.,0.866025403784439));
#19281=DIRECTION('',(0.,-1.,0.));
#19282=DIRECTION('',(-0.5,0.,-0.866025403784439));
#19283=DIRECTION('center_axis',(-1.60246890531964E-16,0.,1.));
#19284=DIRECTION('ref_axis',(-1.,0.,-1.60246890531964E-16));
#19285=DIRECTION('',(1.,0.,1.60246890531964E-16));
#19286=DIRECTION('',(0.,-1.,0.));
#19287=DIRECTION('',(-1.,0.,-1.60246890531964E-16));
#19288=DIRECTION('center_axis',(0.866025403784439,0.,0.5));
#19289=DIRECTION('ref_axis',(-0.5,0.,0.866025403784439));
#19290=DIRECTION('',(0.5,0.,-0.866025403784439));
#19291=DIRECTION('',(-0.5,0.,0.866025403784439));
#19292=DIRECTION('center_axis',(0.,1.,0.));
#19293=DIRECTION('ref_axis',(1.,0.,0.));
#19294=DIRECTION('center_axis',(0.,-1.,0.));
#19295=DIRECTION('ref_axis',(0.,0.,-1.));
#23394=CARTESIAN_POINT('',(0.,0.,0.));
#23395=CARTESIAN_POINT('Origin',(0.3,0.4,0.));
#23396=CARTESIAN_POINT('',(-0.3,0.4,-3.67394039744206E-17));
#23397=CARTESIAN_POINT('Origin',(0.,0.4,0.));
#23398=CARTESIAN_POINT('Origin',(0.,0.375,0.));
#23399=CARTESIAN_POINT('',(-0.35,0.35,-4.28626379701573E-17));
#23400=CARTESIAN_POINT('Origin',(0.,0.35,0.));
#23401=CARTESIAN_POINT('',(-0.325,0.375,-3.9801020972289E-17));
#23402=CARTESIAN_POINT('Origin',(0.,0.19,0.));
#23403=CARTESIAN_POINT('',(-0.35,0.03,-4.28626379701574E-17));
#23404=CARTESIAN_POINT('Origin',(0.,0.03,0.));
#23405=CARTESIAN_POINT('',(-0.35,0.19,-4.28626379701574E-17));
#23406=CARTESIAN_POINT('Origin',(0.,0.0149999999999999,0.));
#23407=CARTESIAN_POINT('',(-0.32,-3.29597460435593E-17,-3.91886975727153E-17));
#23408=CARTESIAN_POINT('Origin',(0.,0.,0.));
#23409=CARTESIAN_POINT('',(-0.335,0.0149999999999999,-4.10256677714363E-17));
#23410=CARTESIAN_POINT('Origin',(0.22,0.,0.));
#23411=CARTESIAN_POINT('',(-0.22,-6.93889390390723E-18,-2.69422295812418E-17));
#23412=CARTESIAN_POINT('Origin',(0.,0.,0.));
#23413=CARTESIAN_POINT('Origin',(0.,-0.02,0.));
#23414=CARTESIAN_POINT('',(-0.1954,-0.0492,2.39295984553393E-17));
#23415=CARTESIAN_POINT('Origin',(0.,-0.0492,0.));
#23416=CARTESIAN_POINT('',(-0.21,-0.02,-2.57175827820944E-17));
#23417=CARTESIAN_POINT('Origin',(0.,-0.8,0.));
#23418=CARTESIAN_POINT('',(-0.1954,-1.5646,2.39295984553393E-17));
#23419=CARTESIAN_POINT('Origin',(0.,-1.5646,0.));
#23420=CARTESIAN_POINT('',(-0.1954,-0.8,-2.39295984553393E-17));
#23421=CARTESIAN_POINT('Origin',(0.,-1.58,0.));
#23422=CARTESIAN_POINT('',(-0.16,-1.6,-1.95943487863577E-17));
#23423=CARTESIAN_POINT('Origin',(0.,-1.6,0.));
#23424=CARTESIAN_POINT('',(-0.18,-1.58,-2.20436423846524E-17));
#23425=CARTESIAN_POINT('Origin',(0.,-1.6,0.));
#23426=CARTESIAN_POINT('Origin',(0.0866025403784439,-0.4,-0.15));
#23427=CARTESIAN_POINT('',(0.173205080756888,-0.4,0.));
#23428=CARTESIAN_POINT('',(0.0866025403784439,-0.4,-0.15));
#23429=CARTESIAN_POINT('',(0.173205080756888,-0.4,0.));
#23430=CARTESIAN_POINT('',(0.0866025403784439,-0.64,-0.15));
#23431=CARTESIAN_POINT('',(0.0866025403784439,-0.4,-0.15));
#23432=CARTESIAN_POINT('',(0.173205080756888,-0.64,0.));
#23433=CARTESIAN_POINT('',(0.173205080756888,-0.64,0.));
#23434=CARTESIAN_POINT('',(0.173205080756888,-0.4,0.));
#23435=CARTESIAN_POINT('Origin',(-0.0866025403784438,-0.4,-0.15));
#23436=CARTESIAN_POINT('',(-0.0866025403784438,-0.4,-0.15));
#23437=CARTESIAN_POINT('',(0.0866025403784439,-0.4,-0.15));
#23438=CARTESIAN_POINT('',(-0.0866025403784438,-0.64,-0.15));
#23439=CARTESIAN_POINT('',(-0.0866025403784438,-0.4,-0.15));
#23440=CARTESIAN_POINT('',(0.0866025403784439,-0.64,-0.15));
#23441=CARTESIAN_POINT('Origin',(-0.173205080756888,-0.4,-2.77555756156289E-17));
#23442=CARTESIAN_POINT('',(-0.173205080756888,-0.4,-2.12115047744981E-17));
#23443=CARTESIAN_POINT('',(-0.0866025403784438,-0.4,-0.15));
#23444=CARTESIAN_POINT('',(-0.173205080756888,-0.64,-2.77555756156289E-17));
#23445=CARTESIAN_POINT('',(-0.173205080756888,-0.4,-2.12115047744981E-17));
#23446=CARTESIAN_POINT('',(-0.0866025403784438,-0.64,-0.15));
#23447=CARTESIAN_POINT('Origin',(-0.0866025403784439,-0.4,0.15));
#23448=CARTESIAN_POINT('',(-0.0866025403784439,-0.4,0.15));
#23449=CARTESIAN_POINT('',(-0.173205080756888,-0.4,-2.12115047744981E-17));
#23450=CARTESIAN_POINT('',(-0.0866025403784439,-0.64,0.15));
#23451=CARTESIAN_POINT('',(-0.0866025403784439,-0.4,0.15));
#23452=CARTESIAN_POINT('',(-0.173205080756888,-0.64,-2.12115047744981E-17));
#23453=CARTESIAN_POINT('Origin',(0.0866025403784439,-0.4,0.15));
#23454=CARTESIAN_POINT('',(0.0866025403784439,-0.4,0.15));
#23455=CARTESIAN_POINT('',(-0.0866025403784439,-0.4,0.15));
#23456=CARTESIAN_POINT('',(0.0866025403784439,-0.64,0.15));
#23457=CARTESIAN_POINT('',(0.0866025403784439,-0.4,0.15));
#23458=CARTESIAN_POINT('',(-0.0866025403784439,-0.64,0.15));
#23459=CARTESIAN_POINT('Origin',(0.173205080756888,-0.4,0.));
#23460=CARTESIAN_POINT('',(0.0866025403784439,-0.4,0.15));
#23461=CARTESIAN_POINT('',(0.0866025403784439,-0.64,0.15));
#23462=CARTESIAN_POINT('Origin',(0.,-0.4,-2.77555756156289E-17));
#23463=CARTESIAN_POINT('Origin',(0.,-0.64,-2.77555756156289E-17));
#24938=UNCERTAINTY_MEASURE_WITH_UNIT(LENGTH_MEASURE(0.001),#25101,
'DISTANCE_ACCURACY_VALUE',
'Maximum model space distance between geometric entities at asserted c
onnectivities');
#24979=UNCERTAINTY_MEASURE_WITH_UNIT(LENGTH_MEASURE(0.001),#25101,
'DISTANCE_ACCURACY_VALUE',
'Maximum model space distance between geometric entities at asserted c
onnectivities');
#25059=(
GEOMETRIC_REPRESENTATION_CONTEXT(3)
GLOBAL_UNCERTAINTY_ASSIGNED_CONTEXT((#24938))
GLOBAL_UNIT_ASSIGNED_CONTEXT((#25101,#25103,#25104))
REPRESENTATION_CONTEXT('','3D')
);
#25100=(
GEOMETRIC_REPRESENTATION_CONTEXT(3)
GLOBAL_UNCERTAINTY_ASSIGNED_CONTEXT((#24979))
GLOBAL_UNIT_ASSIGNED_CONTEXT((#25101,#25103,#25104))
REPRESENTATION_CONTEXT('','3D')
);
#25101=(
LENGTH_UNIT()
NAMED_UNIT(*)
SI_UNIT(.CENTI.,.METRE.)
);
#25103=(
NAMED_UNIT(*)
PLANE_ANGLE_UNIT()
SI_UNIT($,.RADIAN.)
);
#25104=(
NAMED_UNIT(*)
SI_UNIT($,.STERADIAN.)
SOLID_ANGLE_UNIT()
);
#25184=SHAPE_DEFINITION_REPRESENTATION(#25306,#25589);
#25306=PRODUCT_DEFINITION_SHAPE('',$,#25710);
#25589=SHAPE_REPRESENTATION('',(#15673),#25059);
#25630=PRODUCT_DEFINITION_CONTEXT('part definition',#25992,'design');
#25710=PRODUCT_DEFINITION('Cap Screw - M4x16','Cap Screw - M4x16',#25830,
#25630);
#25830=PRODUCT_DEFINITION_FORMATION('',$,#26073);
#25992=APPLICATION_CONTEXT(
'Core Data for Automotive Mechanical Design Process');
#25993=PRODUCT_CONTEXT('part definition',#25992,'mechanical');
#26073=PRODUCT('Cap Screw - M4x16','Cap Screw - M4x16',
'Cap Screw - M4x16',(#25993));
#26192=COLOUR_RGB('Black',0.12,0.14,0.17);
#26193=FILL_AREA_STYLE_COLOUR('',#26192);
#26194=FILL_AREA_STYLE('',(#26193));
#26195=SURFACE_STYLE_FILL_AREA(#26194);
#26196=SURFACE_SIDE_STYLE('',(#26195));
#26197=SURFACE_STYLE_USAGE(.BOTH.,#26196);
#26198=PRESENTATION_STYLE_ASSIGNMENT((#26197));
ENDSEC;
END-ISO-10303-21;
